ISO-10303-21;
HEADER;
/* Generated by software containing ST-Developer
 * from STEP Tools, Inc. (www.steptools.com) 
 */

FILE_DESCRIPTION(
/* description */ ('PAT-001'),
/* implementation_level */ '2;1');

FILE_NAME(
/* name */ 'Flat Washer - M5.step',
/* time_stamp */ '2026-10-29T17:07:15-07:00',
/* author */ (''),
/* organization */ (''),
/* preprocessor_version */ 'ST-DEVELOPER v20.2',
/* originating_system */ 'Autodesk Translation Framework v15.17.0.0',
/* authorisation */ '');

FILE_SCHEMA (('AUTOMOTIVE_DESIGN { 1 0 10303 214 3 1 1 }'));
ENDSEC;

DATA;
#10=MECHANICAL_DESIGN_GEOMETRIC_PRESENTATION_REPRESENTATION('',(#397),#9622);
#309=CONICAL_SURFACE('',#5879,0.275,0.785398163397449);
#339=SHAPE_REPRESENTATION_RELATIONSHIP('SRR','None',#9763,#364);
#364=ADVANCED_BREP_SHAPE_REPRESENTATION('',(#430),#9612);
#397=STYLED_ITEM('',(#9969),#430);
#430=MANIFOLD_SOLID_BREP('Body1',#5222);
#487=FACE_BOUND('',#1267,.T.);
#488=FACE_BOUND('',#1270,.T.);
#664=PLANE('',#5884);
#665=PLANE('',#5888);
#918=FACE_OUTER_BOUND('',#1264,.T.);
#919=FACE_OUTER_BOUND('',#1265,.T.);
#920=FACE_OUTER_BOUND('',#1266,.T.);
#921=FACE_OUTER_BOUND('',#1268,.T.);
#922=FACE_OUTER_BOUND('',#1269,.T.);
#1264=EDGE_LOOP('',(#4455,#4456,#4457,#4458));
#1265=EDGE_LOOP('',(#4459,#4460,#4461,#4462));
#1266=EDGE_LOOP('',(#4463));
#1267=EDGE_LOOP('',(#4464));
#1268=EDGE_LOOP('',(#4465,#4466,#4467,#4468));
#1269=EDGE_LOOP('',(#4469));
#1270=EDGE_LOOP('',(#4470));
#1707=LINE('',#9069,#2112);
#1708=LINE('',#9073,#2113);
#1709=LINE('',#9080,#2114);
#2112=VECTOR('',#7160,0.275);
#2113=VECTOR('',#7165,0.265);
#2114=VECTOR('',#7174,0.5);
#2348=CIRCLE('',#5880,0.285);
#2349=CIRCLE('',#5881,0.265);
#2350=CIRCLE('',#5883,0.265);
#2351=CIRCLE('',#5885,0.5);
#2352=CIRCLE('',#5887,0.5);
#2742=VERTEX_POINT('',#9066);
#2743=VERTEX_POINT('',#9068);
#2744=VERTEX_POINT('',#9072);
#2745=VERTEX_POINT('',#9076);
#2746=VERTEX_POINT('',#9079);
#3331=EDGE_CURVE('',#2742,#2742,#2348,.T.);
#3332=EDGE_CURVE('',#2742,#2743,#1707,.T.);
#3333=EDGE_CURVE('',#2743,#2743,#2349,.T.);
#3334=EDGE_CURVE('',#2743,#2744,#1708,.T.);
#3335=EDGE_CURVE('',#2744,#2744,#2350,.T.);
#3336=EDGE_CURVE('',#2745,#2745,#2351,.T.);
#3337=EDGE_CURVE('',#2745,#2746,#1709,.T.);
#3338=EDGE_CURVE('',#2746,#2746,#2352,.T.);
#4455=ORIENTED_EDGE('',*,*,#3331,.T.);
#4456=ORIENTED_EDGE('',*,*,#3332,.T.);
#4457=ORIENTED_EDGE('',*,*,#3333,.T.);
#4458=ORIENTED_EDGE('',*,*,#3332,.F.);
#4459=ORIENTED_EDGE('',*,*,#3333,.F.);
#4460=ORIENTED_EDGE('',*,*,#3334,.T.);
#4461=ORIENTED_EDGE('',*,*,#3335,.T.);
#4462=ORIENTED_EDGE('',*,*,#3334,.F.);
#4463=ORIENTED_EDGE('',*,*,#3336,.T.);
#4464=ORIENTED_EDGE('',*,*,#3331,.F.);
#4465=ORIENTED_EDGE('',*,*,#3336,.F.);
#4466=ORIENTED_EDGE('',*,*,#3337,.T.);
#4467=ORIENTED_EDGE('',*,*,#3338,.T.);
#4468=ORIENTED_EDGE('',*,*,#3337,.F.);
#4469=ORIENTED_EDGE('',*,*,#3338,.F.);
#4470=ORIENTED_EDGE('',*,*,#3335,.F.);
#4872=CYLINDRICAL_SURFACE('',#5882,0.265);
#4873=CYLINDRICAL_SURFACE('',#5886,0.5);
#5105=ADVANCED_FACE('',(#918),#309,.F.);
#5106=ADVANCED_FACE('',(#919),#4872,.F.);
#5107=ADVANCED_FACE('',(#920,#487),#664,.T.);
#5108=ADVANCED_FACE('',(#921),#4873,.T.);
#5109=ADVANCED_FACE('',(#922,#488),#665,.F.);
#5222=CLOSED_SHELL('',(#5105,#5106,#5107,#5108,#5109));
#5878=AXIS2_PLACEMENT_3D('',#9064,#7154,#7155);
#5879=AXIS2_PLACEMENT_3D('',#9065,#7156,#7157);
#5880=AXIS2_PLACEMENT_3D('',#9067,#7158,#7159);
#5881=AXIS2_PLACEMENT_3D('',#9070,#7161,#7162);
#5882=AXIS2_PLACEMENT_3D('',#9071,#7163,#7164);
#5883=AXIS2_PLACEMENT_3D('',#9074,#7166,#7167);
#5884=AXIS2_PLACEMENT_3D('',#9075,#7168,#7169);
#5885=AXIS2_PLACEMENT_3D('',#9077,#7170,#7171);
#5886=AXIS2_PLACEMENT_3D('',#9078,#7172,#7173);
#5887=AXIS2_PLACEMENT_3D('',#9081,#7175,#7176);
#5888=AXIS2_PLACEMENT_3D('',#9082,#7177,#7178);
#7154=DIRECTION('axis',(0.,0.,1.));
#7155=DIRECTION('refdir',(1.,0.,0.));
#7156=DIRECTION('center_axis',(0.,1.,0.));
#7157=DIRECTION('ref_axis',(1.,0.,0.));
#7158=DIRECTION('center_axis',(0.,1.,0.));
#7159=DIRECTION('ref_axis',(1.,0.,0.));
#7160=DIRECTION('',(0.707106781186548,-0.707106781186547,-8.65956056235494E-17));
#7161=DIRECTION('center_axis',(0.,-1.,0.));
#7162=DIRECTION('ref_axis',(1.,0.,0.));
#7163=DIRECTION('center_axis',(0.,1.,0.));
#7164=DIRECTION('ref_axis',(1.,0.,0.));
#7165=DIRECTION('',(0.,-1.,0.));
#7166=DIRECTION('center_axis',(0.,-1.,0.));
#7167=DIRECTION('ref_axis',(1.,0.,0.));
#7168=DIRECTION('center_axis',(0.,1.,0.));
#7169=DIRECTION('ref_axis',(1.,0.,0.));
#7170=DIRECTION('center_axis',(0.,1.,0.));
#7171=DIRECTION('ref_axis',(1.,0.,0.));
#7172=DIRECTION('center_axis',(0.,1.,0.));
#7173=DIRECTION('ref_axis',(1.,0.,0.));
#7174=DIRECTION('',(0.,-1.,0.));
#7175=DIRECTION('center_axis',(0.,1.,0.));
#7176=DIRECTION('ref_axis',(1.,0.,0.));
#7177=DIRECTION('center_axis',(0.,1.,0.));
#7178=DIRECTION('ref_axis',(1.,0.,0.));
#9064=CARTESIAN_POINT('',(0.,0.,0.));
#9065=CARTESIAN_POINT('Origin',(0.,0.09,0.));
#9066=CARTESIAN_POINT('',(-0.285,0.1,3.49024337756996E-17));
#9067=CARTESIAN_POINT('Origin',(0.,0.1,0.));
#9068=CARTESIAN_POINT('',(-0.265,0.08,-3.24531401774049E-17));
#9069=CARTESIAN_POINT('',(-0.275,0.09,3.36777869765522E-17));
#9070=CARTESIAN_POINT('Origin',(0.,0.08,0.));
#9071=CARTESIAN_POINT('Origin',(0.,0.,0.));
#9072=CARTESIAN_POINT('',(-0.265,0.,3.24531401774049E-17));
#9073=CARTESIAN_POINT('',(-0.265,0.,3.24531401774049E-17));
#9074=CARTESIAN_POINT('Origin',(0.,0.,0.));
#9075=CARTESIAN_POINT('Origin',(0.,0.1,0.));
#9076=CARTESIAN_POINT('',(-0.5,0.1,6.12323399573677E-17));
#9077=CARTESIAN_POINT('Origin',(0.,0.1,0.));
#9078=CARTESIAN_POINT('Origin',(0.,0.,0.));
#9079=CARTESIAN_POINT('',(-0.5,0.,6.12323399573677E-17));
#9080=CARTESIAN_POINT('',(-0.5,0.,6.12323399573677E-17));
#9081=CARTESIAN_POINT('Origin',(0.,0.,0.));
#9082=CARTESIAN_POINT('Origin',(0.,0.,0.));
#9582=UNCERTAINTY_MEASURE_WITH_UNIT(LENGTH_MEASURE(0.001),#9623,
'DISTANCE_ACCURACY_VALUE',
'Maximum model space distance between geometric entities at asserted c
onnectivities');
#9592=UNCERTAINTY_MEASURE_WITH_UNIT(LENGTH_MEASURE(0.001),#9623,
'DISTANCE_ACCURACY_VALUE',
'Maximum model space distance between geometric entities at asserted c
onnectivities');
#9612=(
GEOMETRIC_REPRESENTATION_CONTEXT(3)
GLOBAL_UNCERTAINTY_ASSIGNED_CONTEXT((#9582))
GLOBAL_UNIT_ASSIGNED_CONTEXT((#9623,#9625,#9626))
REPRESENTATION_CONTEXT('','3D')
);
#9622=(
GEOMETRIC_REPRESENTATION_CONTEXT(3)
GLOBAL_UNCERTAINTY_ASSIGNED_CONTEXT((#9592))
GLOBAL_UNIT_ASSIGNED_CONTEXT((#9623,#9625,#9626))
REPRESENTATION_CONTEXT('','3D')
);
#9623=(
LENGTH_UNIT()
NAMED_UNIT(*)
SI_UNIT(.CENTI.,.METRE.)
);
#9625=(
NAMED_UNIT(*)
PLANE_ANGLE_UNIT()
SI_UNIT($,.RADIAN.)
);
#9626=(
NAMED_UNIT(*)
SI_UNIT($,.STERADIAN.)
SOLID_ANGLE_UNIT()
);
#9646=SHAPE_DEFINITION_REPRESENTATION(#9680,#9763);
#9680=PRODUCT_DEFINITION_SHAPE('',$,#9793);
#9763=SHAPE_REPRESENTATION('',(#5878),#9612);
#9773=PRODUCT_DEFINITION_CONTEXT('part definition',#9862,'design');
#9793=PRODUCT_DEFINITION('Flat Washer - M5','Flat Washer - M5',#9822,#9773);
#9822=PRODUCT_DEFINITION_FORMATION('',$,#9883);
#9862=APPLICATION_CONTEXT(
'Core Data for Automotive Mechanical Design Process');
#9863=PRODUCT_CONTEXT('part definition',#9862,'mechanical');
#9883=PRODUCT('Flat Washer - M5','Flat Washer - M5','Flat Washer - M5',
(#9863));
#9963=COLOUR_RGB('Black',0.12,0.14,0.17);
#9964=FILL_AREA_STYLE_COLOUR('',#9963);
#9965=FILL_AREA_STYLE('',(#9964));
#9966=SURFACE_STYLE_FILL_AREA(#9965);
#9967=SURFACE_SIDE_STYLE('',(#9966));
#9968=SURFACE_STYLE_USAGE(.BOTH.,#9967);
#9969=PRESENTATION_STYLE_ASSIGNMENT((#9968));
ENDSEC;
END-ISO-10303-21;
